ISO-10303-21;
HEADER;
/* Generated by software containing ST-Developer
 * from STEP Tools, Inc. (www.steptools.com) 
 */

FILE_DESCRIPTION(
/* description */ ('STEP AP214'),
/* implementation_level */ '2;1');

FILE_NAME(
/* name */ 'PUR-HW-4062.step',
/* time_stamp */ '2026-10-07T12:49:37-07:00',
/* author */ (''),
/* organization */ (''),
/* preprocessor_version */ 'ST-DEVELOPER v20.2',
/* originating_system */ 'Autodesk Translation Framework v15.15.0.0',
/* authorisation */ '');

FILE_SCHEMA (('AUTOMOTIVE_DESIGN { 1 0 10303 214 3 1 1 }'));
ENDSEC;

DATA;
#10=MECHANICAL_DESIGN_GEOMETRIC_PRESENTATION_REPRESENTATION('',(#306),#33016);
#248=SHAPE_REPRESENTATION_RELATIONSHIP('SRR','None',#33142,#275);
#275=ADVANCED_BREP_SHAPE_REPRESENTATION('',(#333),#33003);
#306=STYLED_ITEM('',(#33286),#333);
#333=MANIFOLD_SOLID_BREP('Body1',#9957);
#392=TOROIDAL_SURFACE('',#10869,10.575,0.375000000000001);
#958=PLANE('',#10873);
#959=PLANE('',#10874);
#1390=FACE_OUTER_BOUND('',#1994,.T.);
#1391=FACE_OUTER_BOUND('',#1995,.T.);
#1392=FACE_OUTER_BOUND('',#1996,.T.);
#1994=EDGE_LOOP('',(#8294,#8295,#8296,#8297));
#1995=EDGE_LOOP('',(#8298));
#1996=EDGE_LOOP('',(#8299));
#2459=CIRCLE('',#10870,0.375000000000001);
#2460=CIRCLE('',#10871,10.2);
#2461=CIRCLE('',#10872,0.375000000000001);
#4715=VERTEX_POINT('',#27953);
#4716=VERTEX_POINT('',#27955);
#5960=EDGE_CURVE('',#4715,#4715,#2459,.T.);
#5961=EDGE_CURVE('',#4715,#4716,#2460,.T.);
#5962=EDGE_CURVE('',#4716,#4716,#2461,.T.);
#8294=ORIENTED_EDGE('',*,*,#5960,.T.);
#8295=ORIENTED_EDGE('',*,*,#5961,.T.);
#8296=ORIENTED_EDGE('',*,*,#5962,.F.);
#8297=ORIENTED_EDGE('',*,*,#5961,.F.);
#8298=ORIENTED_EDGE('',*,*,#5962,.T.);
#8299=ORIENTED_EDGE('',*,*,#5960,.F.);
#9756=ADVANCED_FACE('',(#1390),#392,.T.);
#9757=ADVANCED_FACE('',(#1391),#958,.T.);
#9758=ADVANCED_FACE('',(#1392),#959,.F.);
#9957=CLOSED_SHELL('',(#9756,#9757,#9758));
#10868=AXIS2_PLACEMENT_3D('',#27951,#13012,#13013);
#10869=AXIS2_PLACEMENT_3D('',#27952,#13014,#13015);
#10870=AXIS2_PLACEMENT_3D('',#27954,#13016,#13017);
#10871=AXIS2_PLACEMENT_3D('',#27956,#13018,#13019);
#10872=AXIS2_PLACEMENT_3D('',#27957,#13020,#13021);
#10873=AXIS2_PLACEMENT_3D('',#27958,#13022,#13023);
#10874=AXIS2_PLACEMENT_3D('',#27959,#13024,#13025);
#13012=DIRECTION('axis',(0.,0.,1.));
#13013=DIRECTION('refdir',(1.,0.,0.));
#13014=DIRECTION('center_axis',(0.,0.,1.));
#13015=DIRECTION('ref_axis',(1.,0.,0.));
#13016=DIRECTION('center_axis',(0.,1.,0.));
#13017=DIRECTION('ref_axis',(0.,0.,1.));
#13018=DIRECTION('center_axis',(0.,0.,-1.));
#13019=DIRECTION('ref_axis',(1.,0.,0.));
#13020=DIRECTION('center_axis',(-0.173648177666917,0.98480775301221,0.));
#13021=DIRECTION('ref_axis',(0.,0.,1.));
#13022=DIRECTION('center_axis',(-0.173648177666917,0.98480775301221,0.));
#13023=DIRECTION('ref_axis',(0.,0.,1.));
#13024=DIRECTION('center_axis',(0.,1.,0.));
#13025=DIRECTION('ref_axis',(0.,0.,1.));
#27951=CARTESIAN_POINT('',(0.,0.,0.));
#27952=CARTESIAN_POINT('Origin',(0.,0.,0.));
#27953=CARTESIAN_POINT('',(-10.2,0.,-4.59242549680259E-17));
#27954=CARTESIAN_POINT('Origin',(-10.575,0.,0.));
#27955=CARTESIAN_POINT('',(-10.0450390807245,-1.77121141220256,-4.59242549680259E-17));
#27956=CARTESIAN_POINT('Origin',(0.,0.,-4.59242549680259E-17));
#27957=CARTESIAN_POINT('Origin',(-10.4143419881041,-1.83632947882765,0.));
#27958=CARTESIAN_POINT('Origin',(-10.4143419881041,-1.83632947882765,0.));
#27959=CARTESIAN_POINT('Origin',(-10.575,0.,0.));
#32971=UNCERTAINTY_MEASURE_WITH_UNIT(LENGTH_MEASURE(0.01),#33017,
'DISTANCE_ACCURACY_VALUE',
'Maximum model space distance between geometric entities at asserted c
onnectivities');
#32984=UNCERTAINTY_MEASURE_WITH_UNIT(LENGTH_MEASURE(0.01),#33017,
'DISTANCE_ACCURACY_VALUE',
'Maximum model space distance between geometric entities at asserted c
onnectivities');
#33003=(
GEOMETRIC_REPRESENTATION_CONTEXT(3)
GLOBAL_UNCERTAINTY_ASSIGNED_CONTEXT((#32971))
GLOBAL_UNIT_ASSIGNED_CONTEXT((#33017,#33019,#33020))
REPRESENTATION_CONTEXT('','3D')
);
#33016=(
GEOMETRIC_REPRESENTATION_CONTEXT(3)
GLOBAL_UNCERTAINTY_ASSIGNED_CONTEXT((#32984))
GLOBAL_UNIT_ASSIGNED_CONTEXT((#33017,#33019,#33020))
REPRESENTATION_CONTEXT('','3D')
);
#33017=(
LENGTH_UNIT()
NAMED_UNIT(*)
SI_UNIT(.MILLI.,.METRE.)
);
#33019=(
NAMED_UNIT(*)
PLANE_ANGLE_UNIT()
SI_UNIT($,.RADIAN.)
);
#33020=(
NAMED_UNIT(*)
SI_UNIT($,.STERADIAN.)
SOLID_ANGLE_UNIT()
);
#33039=SHAPE_DEFINITION_REPRESENTATION(#33078,#33142);
#33078=PRODUCT_DEFINITION_SHAPE('',$,#33174);
#33142=SHAPE_REPRESENTATION('',(#10868),#33003);
#33155=PRODUCT_DEFINITION_CONTEXT('part definition',#33250,'design');
#33174=PRODUCT_DEFINITION(
'P_Torque Wrench_External C-Clip_PUR-HW-4062_M_Rev00','PUR-HW-4062',#33205,
#33155);
#33205=PRODUCT_DEFINITION_FORMATION('',$,#33270);
#33250=APPLICATION_CONTEXT(
'Core Data for Automotive Mechanical Design Process');
#33251=PRODUCT_CONTEXT('part definition',#33250,'mechanical');
#33270=PRODUCT('P_Torque Wrench_External C-Clip_PUR-HW-4062_M_Rev00',
'PUR-HW-4062',$,(#33251));
#33286=PRESENTATION_STYLE_ASSIGNMENT((#33293));
#33293=SURFACE_STYLE_USAGE(.BOTH.,#33300);
#33300=SURFACE_SIDE_STYLE('',(#33307));
#33307=SURFACE_STYLE_FILL_AREA(#33314);
#33314=FILL_AREA_STYLE('Opaque(178,178,178)',(#33321));
#33321=FILL_AREA_STYLE_COLOUR('Opaque(178,178,178)',#33328);
#33328=COLOUR_RGB('Opaque(178,178,178)', 0.66274510, 0.83137255, 0.94901961);
ENDSEC;
END-ISO-10303-21;
